ISO-10303-21;
HEADER;
/* Generated by software containing ST-Developer
 * from STEP Tools, Inc. (www.steptools.com) 
 */

FILE_DESCRIPTION(
/* description */ ('PAT-097'),
/* implementation_level */ '2;1');

FILE_NAME(
/* name */ 'Flat Washer - M8.step',
/* time_stamp */ '2026-10-29T15:59:31-07:00',
/* author */ (''),
/* organization */ (''),
/* preprocessor_version */ 'ST-DEVELOPER v20.2',
/* originating_system */ 'Autodesk Translation Framework v15.17.0.0',
/* authorisation */ '');

FILE_SCHEMA (('AUTOMOTIVE_DESIGN { 1 0 10303 214 3 1 1 }'));
ENDSEC;

DATA;
#10=MECHANICAL_DESIGN_GEOMETRIC_PRESENTATION_REPRESENTATION('',(#80),#2768);
#66=SHAPE_REPRESENTATION_RELATIONSHIP('SRR','None',#2804,#73);
#73=ADVANCED_BREP_SHAPE_REPRESENTATION('',(#87),#2766);
#80=STYLED_ITEM('',(#2918),#87);
#87=MANIFOLD_SOLID_BREP('Body1',#1601);
#113=CYLINDRICAL_SURFACE('',#1804,0.42);
#114=CYLINDRICAL_SURFACE('',#1807,0.8);
#160=FACE_BOUND('',#418,.T.);
#161=FACE_BOUND('',#420,.T.);
#212=CIRCLE('',#1805,0.42);
#213=CIRCLE('',#1806,0.42);
#214=CIRCLE('',#1808,0.8);
#215=CIRCLE('',#1809,0.8);
#288=FACE_OUTER_BOUND('',#415,.T.);
#289=FACE_OUTER_BOUND('',#416,.T.);
#290=FACE_OUTER_BOUND('',#417,.T.);
#291=FACE_OUTER_BOUND('',#419,.T.);
#415=EDGE_LOOP('',(#1397,#1398,#1399,#1400));
#416=EDGE_LOOP('',(#1401,#1402,#1403,#1404));
#417=EDGE_LOOP('',(#1405));
#418=EDGE_LOOP('',(#1406));
#419=EDGE_LOOP('',(#1407));
#420=EDGE_LOOP('',(#1408));
#560=LINE('',#2655,#697);
#561=LINE('',#2661,#698);
#697=VECTOR('',#2213,0.42);
#698=VECTOR('',#2220,0.8);
#824=VERTEX_POINT('',#2652);
#825=VERTEX_POINT('',#2654);
#826=VERTEX_POINT('',#2658);
#827=VERTEX_POINT('',#2660);
#1018=EDGE_CURVE('',#824,#824,#212,.T.);
#1019=EDGE_CURVE('',#824,#825,#560,.T.);
#1020=EDGE_CURVE('',#825,#825,#213,.T.);
#1021=EDGE_CURVE('',#826,#826,#214,.T.);
#1022=EDGE_CURVE('',#826,#827,#561,.T.);
#1023=EDGE_CURVE('',#827,#827,#215,.T.);
#1397=ORIENTED_EDGE('',*,*,#1018,.F.);
#1398=ORIENTED_EDGE('',*,*,#1019,.T.);
#1399=ORIENTED_EDGE('',*,*,#1020,.T.);
#1400=ORIENTED_EDGE('',*,*,#1019,.F.);
#1401=ORIENTED_EDGE('',*,*,#1021,.F.);
#1402=ORIENTED_EDGE('',*,*,#1022,.T.);
#1403=ORIENTED_EDGE('',*,*,#1023,.T.);
#1404=ORIENTED_EDGE('',*,*,#1022,.F.);
#1405=ORIENTED_EDGE('',*,*,#1021,.T.);
#1406=ORIENTED_EDGE('',*,*,#1018,.T.);
#1407=ORIENTED_EDGE('',*,*,#1023,.F.);
#1408=ORIENTED_EDGE('',*,*,#1020,.F.);
#1503=PLANE('',#1810);
#1504=PLANE('',#1811);
#1581=ADVANCED_FACE('',(#288),#113,.F.);
#1582=ADVANCED_FACE('',(#289),#114,.T.);
#1583=ADVANCED_FACE('',(#290,#160),#1503,.T.);
#1584=ADVANCED_FACE('',(#291,#161),#1504,.F.);
#1601=CLOSED_SHELL('',(#1581,#1582,#1583,#1584));
#1803=AXIS2_PLACEMENT_3D('',#2650,#2207,#2208);
#1804=AXIS2_PLACEMENT_3D('',#2651,#2209,#2210);
#1805=AXIS2_PLACEMENT_3D('',#2653,#2211,#2212);
#1806=AXIS2_PLACEMENT_3D('',#2656,#2214,#2215);
#1807=AXIS2_PLACEMENT_3D('',#2657,#2216,#2217);
#1808=AXIS2_PLACEMENT_3D('',#2659,#2218,#2219);
#1809=AXIS2_PLACEMENT_3D('',#2662,#2221,#2222);
#1810=AXIS2_PLACEMENT_3D('',#2663,#2223,#2224);
#1811=AXIS2_PLACEMENT_3D('',#2664,#2225,#2226);
#2207=DIRECTION('axis',(0.,0.,1.));
#2208=DIRECTION('refdir',(1.,0.,0.));
#2209=DIRECTION('center_axis',(0.,1.,0.));
#2210=DIRECTION('ref_axis',(1.,0.,0.));
#2211=DIRECTION('center_axis',(0.,-1.,0.));
#2212=DIRECTION('ref_axis',(1.,0.,0.));
#2213=DIRECTION('',(0.,-1.,0.));
#2214=DIRECTION('center_axis',(0.,-1.,0.));
#2215=DIRECTION('ref_axis',(1.,0.,0.));
#2216=DIRECTION('center_axis',(0.,1.,0.));
#2217=DIRECTION('ref_axis',(1.,0.,0.));
#2218=DIRECTION('center_axis',(0.,1.,0.));
#2219=DIRECTION('ref_axis',(1.,0.,0.));
#2220=DIRECTION('',(0.,-1.,0.));
#2221=DIRECTION('center_axis',(0.,1.,0.));
#2222=DIRECTION('ref_axis',(1.,0.,0.));
#2223=DIRECTION('center_axis',(0.,1.,0.));
#2224=DIRECTION('ref_axis',(1.,0.,0.));
#2225=DIRECTION('center_axis',(0.,1.,0.));
#2226=DIRECTION('ref_axis',(1.,0.,0.));
#2650=CARTESIAN_POINT('',(0.,0.,0.));
#2651=CARTESIAN_POINT('Origin',(0.,0.,0.));
#2652=CARTESIAN_POINT('',(-0.42,0.16,5.14351655641888E-17));
#2653=CARTESIAN_POINT('Origin',(0.,0.16,0.));
#2654=CARTESIAN_POINT('',(-0.42,0.,5.14351655641888E-17));
#2655=CARTESIAN_POINT('',(-0.42,0.,5.14351655641888E-17));
#2656=CARTESIAN_POINT('Origin',(0.,0.,0.));
#2657=CARTESIAN_POINT('Origin',(0.,0.,0.));
#2658=CARTESIAN_POINT('',(-0.8,0.16,9.79717439317883E-17));
#2659=CARTESIAN_POINT('Origin',(0.,0.16,0.));
#2660=CARTESIAN_POINT('',(-0.8,0.,9.79717439317883E-17));
#2661=CARTESIAN_POINT('',(-0.8,0.,9.79717439317883E-17));
#2662=CARTESIAN_POINT('Origin',(0.,0.,0.));
#2663=CARTESIAN_POINT('Origin',(0.,0.16,0.));
#2664=CARTESIAN_POINT('Origin',(0.,0.,0.));
#2757=UNCERTAINTY_MEASURE_WITH_UNIT(LENGTH_MEASURE(0.001),#2769,
'DISTANCE_ACCURACY_VALUE',
'Maximum model space distance between geometric entities at asserted c
onnectivities');
#2759=UNCERTAINTY_MEASURE_WITH_UNIT(LENGTH_MEASURE(0.001),#2769,
'DISTANCE_ACCURACY_VALUE',
'Maximum model space distance between geometric entities at asserted c
onnectivities');
#2766=(
GEOMETRIC_REPRESENTATION_CONTEXT(3)
GLOBAL_UNCERTAINTY_ASSIGNED_CONTEXT((#2757))
GLOBAL_UNIT_ASSIGNED_CONTEXT((#2769,#2771,#2772))
REPRESENTATION_CONTEXT('','3D')
);
#2768=(
GEOMETRIC_REPRESENTATION_CONTEXT(3)
GLOBAL_UNCERTAINTY_ASSIGNED_CONTEXT((#2759))
GLOBAL_UNIT_ASSIGNED_CONTEXT((#2769,#2771,#2772))
REPRESENTATION_CONTEXT('','3D')
);
#2769=(
LENGTH_UNIT()
NAMED_UNIT(*)
SI_UNIT(.CENTI.,.METRE.)
);
#2771=(
NAMED_UNIT(*)
PLANE_ANGLE_UNIT()
SI_UNIT($,.RADIAN.)
);
#2772=(
NAMED_UNIT(*)
SI_UNIT($,.STERADIAN.)
SOLID_ANGLE_UNIT()
);
#2779=SHAPE_DEFINITION_REPRESENTATION(#2787,#2804);
#2787=PRODUCT_DEFINITION_SHAPE('',$,#2813);
#2804=SHAPE_REPRESENTATION('',(#1803),#2766);
#2806=PRODUCT_DEFINITION_CONTEXT('part definition',#2832,'design');
#2813=PRODUCT_DEFINITION('Flat Washer - M8','Flat Washer - M8',
#2821,#2806);
#2821=PRODUCT_DEFINITION_FORMATION('',$,#2840);
#2832=APPLICATION_CONTEXT(
'Core Data for Automotive Mechanical Design Process');
#2833=PRODUCT_CONTEXT('part definition',#2832,'mechanical');
#2840=PRODUCT('Flat Washer - M8','Flat Washer - M8',
'Flat Washer - M8',(#2833));
#2912=COLOUR_RGB('Black',0.12,0.14,0.17);
#2913=FILL_AREA_STYLE_COLOUR('',#2912);
#2914=FILL_AREA_STYLE('',(#2913));
#2915=SURFACE_STYLE_FILL_AREA(#2914);
#2916=SURFACE_SIDE_STYLE('',(#2915));
#2917=SURFACE_STYLE_USAGE(.BOTH.,#2916);
#2918=PRESENTATION_STYLE_ASSIGNMENT((#2917));
ENDSEC;
END-ISO-10303-21;
